ISO-10303-21;
HEADER;
/* Generated by software containing ST-Developer
 * from STEP Tools, Inc. (www.steptools.com) 
 */

FILE_DESCRIPTION(
/* description */ (''),
/* implementation_level */ '2;1');

FILE_NAME(
/* name */ 'Blade_05.step',
/* time_stamp */ '2026-10-23T22:28:14+06:00',
/* author */ (''),
/* organization */ (''),
/* preprocessor_version */ 'ST-DEVELOPER v20.2',
/* originating_system */ 'Autodesk Translation Framework v15.15.0.0',
/* authorisation */ '');

FILE_SCHEMA (('AUTOMOTIVE_DESIGN { 1 0 10303 214 3 1 1 }'));
ENDSEC;

DATA;
#10=MECHANICAL_DESIGN_GEOMETRIC_PRESENTATION_REPRESENTATION('',(#111),#6753);
#85=SHAPE_REPRESENTATION_RELATIONSHIP('SRR','None',#6808,#98);
#98=ADVANCED_BREP_SHAPE_REPRESENTATION('',(#124),#6748);
#111=STYLED_ITEM('',(#6935),#124);
#124=MANIFOLD_SOLID_BREP('Blade_05',#3760);
#176=FACE_BOUND('',#759,.T.);
#177=FACE_BOUND('',#760,.T.);
#303=PLANE('',#4258);
#304=PLANE('',#4259);
#305=PLANE('',#4260);
#306=PLANE('',#4267);
#307=PLANE('',#4270);
#308=PLANE('',#4275);
#496=FACE_OUTER_BOUND('',#756,.T.);
#497=FACE_OUTER_BOUND('',#757,.T.);
#498=FACE_OUTER_BOUND('',#758,.T.);
#499=FACE_OUTER_BOUND('',#761,.T.);
#500=FACE_OUTER_BOUND('',#762,.T.);
#501=FACE_OUTER_BOUND('',#763,.T.);
#502=FACE_OUTER_BOUND('',#764,.T.);
#503=FACE_OUTER_BOUND('',#765,.T.);
#504=FACE_OUTER_BOUND('',#766,.T.);
#505=FACE_OUTER_BOUND('',#767,.T.);
#756=EDGE_LOOP('',(#3298,#3299,#3300,#3301));
#757=EDGE_LOOP('',(#3302,#3303,#3304,#3305));
#758=EDGE_LOOP('',(#3306,#3307,#3308,#3309));
#759=EDGE_LOOP('',(#3310));
#760=EDGE_LOOP('',(#3311));
#761=EDGE_LOOP('',(#3312,#3313,#3314,#3315));
#762=EDGE_LOOP('',(#3316));
#763=EDGE_LOOP('',(#3317,#3318,#3319,#3320));
#764=EDGE_LOOP('',(#3321));
#765=EDGE_LOOP('',(#3322,#3323,#3324,#3325));
#766=EDGE_LOOP('',(#3326,#3327,#3328,#3329));
#767=EDGE_LOOP('',(#3330,#3331,#3332,#3333));
#992=CIRCLE('',#4261,33.8);
#993=CIRCLE('',#4262,4.99999999999999);
#994=CIRCLE('',#4263,1.1);
#995=CIRCLE('',#4264,1.1);
#996=CIRCLE('',#4266,1.1);
#997=CIRCLE('',#4269,1.1);
#998=CIRCLE('',#4272,4.99999999999999);
#999=CIRCLE('',#4274,33.8);
#1268=LINE('',#6510,#1554);
#1269=LINE('',#6512,#1555);
#1270=LINE('',#6514,#1556);
#1271=LINE('',#6515,#1557);
#1272=LINE('',#6519,#1558);
#1273=LINE('',#6521,#1559);
#1274=LINE('',#6523,#1560);
#1275=LINE('',#6524,#1561);
#1276=LINE('',#6535,#1562);
#1277=LINE('',#6540,#1563);
#1554=VECTOR('',#5301,10.);
#1555=VECTOR('',#5302,10.);
#1556=VECTOR('',#5303,10.);
#1557=VECTOR('',#5304,10.);
#1558=VECTOR('',#5307,10.);
#1559=VECTOR('',#5308,10.);
#1560=VECTOR('',#5309,10.);
#1561=VECTOR('',#5310,10.);
#1562=VECTOR('',#5325,1.1);
#1563=VECTOR('',#5332,1.1);
#1885=VERTEX_POINT('',#6508);
#1886=VERTEX_POINT('',#6509);
#1887=VERTEX_POINT('',#6511);
#1888=VERTEX_POINT('',#6513);
#1889=VERTEX_POINT('',#6517);
#1890=VERTEX_POINT('',#6518);
#1891=VERTEX_POINT('',#6520);
#1892=VERTEX_POINT('',#6522);
#1893=VERTEX_POINT('',#6528);
#1894=VERTEX_POINT('',#6530);
#1895=VERTEX_POINT('',#6533);
#1896=VERTEX_POINT('',#6538);
#2366=EDGE_CURVE('',#1885,#1886,#1268,.T.);
#2367=EDGE_CURVE('',#1887,#1885,#1269,.T.);
#2368=EDGE_CURVE('',#1888,#1887,#1270,.T.);
#2369=EDGE_CURVE('',#1886,#1888,#1271,.T.);
#2370=EDGE_CURVE('',#1889,#1890,#1272,.T.);
#2371=EDGE_CURVE('',#1891,#1889,#1273,.T.);
#2372=EDGE_CURVE('',#1892,#1891,#1274,.T.);
#2373=EDGE_CURVE('',#1890,#1892,#1275,.T.);
#2374=EDGE_CURVE('',#1889,#1886,#992,.T.);
#2375=EDGE_CURVE('',#1885,#1890,#993,.T.);
#2376=EDGE_CURVE('',#1893,#1893,#994,.T.);
#2377=EDGE_CURVE('',#1894,#1894,#995,.T.);
#2378=EDGE_CURVE('',#1895,#1895,#996,.T.);
#2379=EDGE_CURVE('',#1895,#1893,#1276,.T.);
#2380=EDGE_CURVE('',#1896,#1896,#997,.T.);
#2381=EDGE_CURVE('',#1896,#1894,#1277,.T.);
#2382=EDGE_CURVE('',#1887,#1892,#998,.T.);
#2383=EDGE_CURVE('',#1891,#1888,#999,.T.);
#3298=ORIENTED_EDGE('',*,*,#2366,.F.);
#3299=ORIENTED_EDGE('',*,*,#2367,.F.);
#3300=ORIENTED_EDGE('',*,*,#2368,.F.);
#3301=ORIENTED_EDGE('',*,*,#2369,.F.);
#3302=ORIENTED_EDGE('',*,*,#2370,.F.);
#3303=ORIENTED_EDGE('',*,*,#2371,.F.);
#3304=ORIENTED_EDGE('',*,*,#2372,.F.);
#3305=ORIENTED_EDGE('',*,*,#2373,.F.);
#3306=ORIENTED_EDGE('',*,*,#2366,.T.);
#3307=ORIENTED_EDGE('',*,*,#2374,.F.);
#3308=ORIENTED_EDGE('',*,*,#2370,.T.);
#3309=ORIENTED_EDGE('',*,*,#2375,.F.);
#3310=ORIENTED_EDGE('',*,*,#2376,.T.);
#3311=ORIENTED_EDGE('',*,*,#2377,.T.);
#3312=ORIENTED_EDGE('',*,*,#2378,.F.);
#3313=ORIENTED_EDGE('',*,*,#2379,.T.);
#3314=ORIENTED_EDGE('',*,*,#2376,.F.);
#3315=ORIENTED_EDGE('',*,*,#2379,.F.);
#3316=ORIENTED_EDGE('',*,*,#2378,.T.);
#3317=ORIENTED_EDGE('',*,*,#2380,.F.);
#3318=ORIENTED_EDGE('',*,*,#2381,.T.);
#3319=ORIENTED_EDGE('',*,*,#2377,.F.);
#3320=ORIENTED_EDGE('',*,*,#2381,.F.);
#3321=ORIENTED_EDGE('',*,*,#2380,.T.);
#3322=ORIENTED_EDGE('',*,*,#2367,.T.);
#3323=ORIENTED_EDGE('',*,*,#2375,.T.);
#3324=ORIENTED_EDGE('',*,*,#2373,.T.);
#3325=ORIENTED_EDGE('',*,*,#2382,.F.);
#3326=ORIENTED_EDGE('',*,*,#2369,.T.);
#3327=ORIENTED_EDGE('',*,*,#2383,.F.);
#3328=ORIENTED_EDGE('',*,*,#2371,.T.);
#3329=ORIENTED_EDGE('',*,*,#2374,.T.);
#3330=ORIENTED_EDGE('',*,*,#2368,.T.);
#3331=ORIENTED_EDGE('',*,*,#2382,.T.);
#3332=ORIENTED_EDGE('',*,*,#2372,.T.);
#3333=ORIENTED_EDGE('',*,*,#2383,.T.);
#3519=CYLINDRICAL_SURFACE('',#4265,1.1);
#3520=CYLINDRICAL_SURFACE('',#4268,1.1);
#3521=CYLINDRICAL_SURFACE('',#4271,4.99999999999999);
#3522=CYLINDRICAL_SURFACE('',#4273,33.8);
#3702=ADVANCED_FACE('',(#496),#303,.F.);
#3703=ADVANCED_FACE('',(#497),#304,.F.);
#3704=ADVANCED_FACE('',(#498,#176,#177),#305,.F.);
#3705=ADVANCED_FACE('',(#499),#3519,.T.);
#3706=ADVANCED_FACE('',(#500),#306,.F.);
#3707=ADVANCED_FACE('',(#501),#3520,.T.);
#3708=ADVANCED_FACE('',(#502),#307,.F.);
#3709=ADVANCED_FACE('',(#503),#3521,.F.);
#3710=ADVANCED_FACE('',(#504),#3522,.T.);
#3711=ADVANCED_FACE('',(#505),#308,.T.);
#3760=CLOSED_SHELL('',(#3702,#3703,#3704,#3705,#3706,#3707,#3708,#3709,
#3710,#3711));
#4257=AXIS2_PLACEMENT_3D('',#6506,#5297,#5298);
#4258=AXIS2_PLACEMENT_3D('',#6507,#5299,#5300);
#4259=AXIS2_PLACEMENT_3D('',#6516,#5305,#5306);
#4260=AXIS2_PLACEMENT_3D('',#6525,#5311,#5312);
#4261=AXIS2_PLACEMENT_3D('',#6526,#5313,#5314);
#4262=AXIS2_PLACEMENT_3D('',#6527,#5315,#5316);
#4263=AXIS2_PLACEMENT_3D('',#6529,#5317,#5318);
#4264=AXIS2_PLACEMENT_3D('',#6531,#5319,#5320);
#4265=AXIS2_PLACEMENT_3D('',#6532,#5321,#5322);
#4266=AXIS2_PLACEMENT_3D('',#6534,#5323,#5324);
#4267=AXIS2_PLACEMENT_3D('',#6536,#5326,#5327);
#4268=AXIS2_PLACEMENT_3D('',#6537,#5328,#5329);
#4269=AXIS2_PLACEMENT_3D('',#6539,#5330,#5331);
#4270=AXIS2_PLACEMENT_3D('',#6541,#5333,#5334);
#4271=AXIS2_PLACEMENT_3D('',#6542,#5335,#5336);
#4272=AXIS2_PLACEMENT_3D('',#6543,#5337,#5338);
#4273=AXIS2_PLACEMENT_3D('',#6544,#5339,#5340);
#4274=AXIS2_PLACEMENT_3D('',#6545,#5341,#5342);
#4275=AXIS2_PLACEMENT_3D('',#6546,#5343,#5344);
#5297=DIRECTION('axis',(0.,0.,1.));
#5298=DIRECTION('refdir',(1.,0.,0.));
#5299=DIRECTION('center_axis',(0.707106781186547,0.,-0.707106781186548));
#5300=DIRECTION('ref_axis',(-0.707106781186548,0.,-0.707106781186547));
#5301=DIRECTION('',(-0.707106781186548,0.,-0.707106781186547));
#5302=DIRECTION('',(0.,-1.,0.));
#5303=DIRECTION('',(0.707106781186548,0.,0.707106781186547));
#5304=DIRECTION('',(0.,1.,0.));
#5305=DIRECTION('center_axis',(-1.,0.,1.22464679914735E-16));
#5306=DIRECTION('ref_axis',(1.22464679914735E-16,0.,1.));
#5307=DIRECTION('',(1.22464679914735E-16,0.,1.));
#5308=DIRECTION('',(0.,-1.,0.));
#5309=DIRECTION('',(-1.22464679914735E-16,0.,-1.));
#5310=DIRECTION('',(0.,1.,0.));
#5311=DIRECTION('center_axis',(0.,1.,0.));
#5312=DIRECTION('ref_axis',(-1.,0.,1.22464679914735E-16));
#5313=DIRECTION('center_axis',(0.,1.,0.));
#5314=DIRECTION('ref_axis',(-1.,0.,1.22464679914735E-16));
#5315=DIRECTION('center_axis',(0.,-1.,0.));
#5316=DIRECTION('ref_axis',(-1.,0.,1.22464679914735E-16));
#5317=DIRECTION('center_axis',(0.,1.,0.));
#5318=DIRECTION('ref_axis',(-1.,0.,1.22464679914735E-16));
#5319=DIRECTION('center_axis',(0.,1.,0.));
#5320=DIRECTION('ref_axis',(-1.,0.,1.22464679914735E-16));
#5321=DIRECTION('center_axis',(0.,-1.,0.));
#5322=DIRECTION('ref_axis',(-1.,0.,1.22464679914735E-16));
#5323=DIRECTION('center_axis',(0.,-1.,0.));
#5324=DIRECTION('ref_axis',(-1.,0.,1.22464679914735E-16));
#5325=DIRECTION('',(0.,1.,0.));
#5326=DIRECTION('center_axis',(0.,1.,0.));
#5327=DIRECTION('ref_axis',(-1.,0.,1.22464679914735E-16));
#5328=DIRECTION('center_axis',(0.,-1.,0.));
#5329=DIRECTION('ref_axis',(-1.,0.,1.22464679914735E-16));
#5330=DIRECTION('center_axis',(0.,-1.,0.));
#5331=DIRECTION('ref_axis',(-1.,0.,1.22464679914735E-16));
#5332=DIRECTION('',(0.,1.,0.));
#5333=DIRECTION('center_axis',(0.,1.,0.));
#5334=DIRECTION('ref_axis',(-1.,0.,1.22464679914735E-16));
#5335=DIRECTION('center_axis',(0.,1.,0.));
#5336=DIRECTION('ref_axis',(-1.,0.,1.22464679914735E-16));
#5337=DIRECTION('center_axis',(0.,-1.,0.));
#5338=DIRECTION('ref_axis',(-1.,0.,1.22464679914735E-16));
#5339=DIRECTION('center_axis',(0.,1.,0.));
#5340=DIRECTION('ref_axis',(-1.,0.,1.22464679914735E-16));
#5341=DIRECTION('center_axis',(0.,1.,0.));
#5342=DIRECTION('ref_axis',(-1.,0.,1.22464679914735E-16));
#5343=DIRECTION('center_axis',(0.,1.,0.));
#5344=DIRECTION('ref_axis',(-1.,0.,1.22464679914735E-16));
#6506=CARTESIAN_POINT('',(0.,0.,0.));
#6507=CARTESIAN_POINT('Origin',(-3.53553390593274,-3.,110.796874251098));
#6508=CARTESIAN_POINT('',(-3.53553390593274,-3.,110.796874251098));
#6509=CARTESIAN_POINT('',(-23.9002092041053,-3.,90.4321989529251));
#6510=CARTESIAN_POINT('',(-1.76776695296637,-3.,112.564641204064));
#6511=CARTESIAN_POINT('',(-3.53553390593274,-2.9,110.796874251098));
#6512=CARTESIAN_POINT('',(-3.53553390593274,-3.,110.796874251098));
#6513=CARTESIAN_POINT('',(-23.9002092041053,-2.9,90.4321989529251));
#6514=CARTESIAN_POINT('',(-1.76776695296637,-2.9,112.564641204064));
#6515=CARTESIAN_POINT('',(-23.9002092041053,-3.,90.4321989529251));
#6516=CARTESIAN_POINT('Origin',(-6.35975223036837E-15,-3.,80.5324081570305));
#6517=CARTESIAN_POINT('',(-6.35975223036837E-15,-3.,80.5324081570305));
#6518=CARTESIAN_POINT('',(-2.83276944882399E-15,-3.,109.33240815703));
#6519=CARTESIAN_POINT('',(-4.29009913980934E-15,-3.,97.4324081570305));
#6520=CARTESIAN_POINT('',(-6.35975223036837E-15,-2.9,80.5324081570305));
#6521=CARTESIAN_POINT('',(-6.35975223036837E-15,-3.,80.5324081570305));
#6522=CARTESIAN_POINT('',(-2.83276944882399E-15,-2.9,109.33240815703));
#6523=CARTESIAN_POINT('',(-4.29009913980934E-15,-2.9,97.4324081570305));
#6524=CARTESIAN_POINT('',(-2.83276944882399E-15,-3.,109.33240815703));
#6525=CARTESIAN_POINT('Origin',(-4.44089209850063E-15,-3.,114.33240815703));
#6526=CARTESIAN_POINT('Origin',(-2.22044604925031E-15,-3.,114.33240815703));
#6527=CARTESIAN_POINT('Origin',(-2.22044604925031E-15,-3.,114.33240815703));
#6528=CARTESIAN_POINT('',(-5.20441727387072,-3.,85.7873857361326));
#6529=CARTESIAN_POINT('Origin',(-6.30441727387072,-3.,85.7873857361326));
#6530=CARTESIAN_POINT('',(-15.6482292407074,-3.,90.3728422287137));
#6531=CARTESIAN_POINT('Origin',(-16.7482292407074,-3.,90.3728422287137));
#6532=CARTESIAN_POINT('Origin',(-6.30441727387072,-3.,85.7873857361326));
#6533=CARTESIAN_POINT('',(-5.20441727387072,-3.5,85.7873857361326));
#6534=CARTESIAN_POINT('Origin',(-6.30441727387072,-3.5,85.7873857361326));
#6535=CARTESIAN_POINT('',(-5.20441727387072,-3.,85.7873857361326));
#6536=CARTESIAN_POINT('Origin',(-6.30441727387072,-3.5,85.7873857361326));
#6537=CARTESIAN_POINT('Origin',(-16.7482292407074,-3.,90.3728422287137));
#6538=CARTESIAN_POINT('',(-15.6482292407074,-3.5,90.3728422287137));
#6539=CARTESIAN_POINT('Origin',(-16.7482292407074,-3.5,90.3728422287137));
#6540=CARTESIAN_POINT('',(-15.6482292407074,-3.,90.3728422287137));
#6541=CARTESIAN_POINT('Origin',(-16.7482292407074,-3.5,90.3728422287137));
#6542=CARTESIAN_POINT('Origin',(-2.22044604925031E-15,-3.,114.33240815703));
#6543=CARTESIAN_POINT('Origin',(-2.22044604925031E-15,-2.9,114.33240815703));
#6544=CARTESIAN_POINT('Origin',(-2.22044604925031E-15,-3.,114.33240815703));
#6545=CARTESIAN_POINT('Origin',(-2.22044604925031E-15,-2.9,114.33240815703));
#6546=CARTESIAN_POINT('Origin',(-4.44089209850063E-15,-2.9,114.33240815703));
#6733=UNCERTAINTY_MEASURE_WITH_UNIT(LENGTH_MEASURE(0.01),#6754,
'DISTANCE_ACCURACY_VALUE',
'Maximum model space distance between geometric entities at asserted c
onnectivities');
#6738=UNCERTAINTY_MEASURE_WITH_UNIT(LENGTH_MEASURE(0.01),#6754,
'DISTANCE_ACCURACY_VALUE',
'Maximum model space distance between geometric entities at asserted c
onnectivities');
#6748=(
GEOMETRIC_REPRESENTATION_CONTEXT(3)
GLOBAL_UNCERTAINTY_ASSIGNED_CONTEXT((#6733))
GLOBAL_UNIT_ASSIGNED_CONTEXT((#6754,#6756,#6757))
REPRESENTATION_CONTEXT('','3D')
);
#6753=(
GEOMETRIC_REPRESENTATION_CONTEXT(3)
GLOBAL_UNCERTAINTY_ASSIGNED_CONTEXT((#6738))
GLOBAL_UNIT_ASSIGNED_CONTEXT((#6754,#6756,#6757))
REPRESENTATION_CONTEXT('','3D')
);
#6754=(
LENGTH_UNIT()
NAMED_UNIT(*)
SI_UNIT(.MILLI.,.METRE.)
);
#6756=(
NAMED_UNIT(*)
PLANE_ANGLE_UNIT()
SI_UNIT($,.RADIAN.)
);
#6757=(
NAMED_UNIT(*)
SI_UNIT($,.STERADIAN.)
SOLID_ANGLE_UNIT()
);
#6767=SHAPE_DEFINITION_REPRESENTATION(#6781,#6808);
#6781=PRODUCT_DEFINITION_SHAPE('',$,#6823);
#6808=SHAPE_REPRESENTATION('',(#4257),#6748);
#6813=PRODUCT_DEFINITION_CONTEXT('part definition',#6857,'design');
#6823=PRODUCT_DEFINITION('Blade_05','Blade_05',#6837,#6813);
#6837=PRODUCT_DEFINITION_FORMATION('',$,#6868);
#6857=APPLICATION_CONTEXT(
'Core Data for Automotive Mechanical Design Process');
#6858=PRODUCT_CONTEXT('part definition',#6857,'mechanical');
#6868=PRODUCT('Blade_05','Blade_05',$,(#6858));
#6929=COLOUR_RGB('Off White',0.89,0.88,0.83);
#6930=FILL_AREA_STYLE_COLOUR('',#6929);
#6931=FILL_AREA_STYLE('',(#6930));
#6932=SURFACE_STYLE_FILL_AREA(#6931);
#6933=SURFACE_SIDE_STYLE('',(#6932));
#6934=SURFACE_STYLE_USAGE(.BOTH.,#6933);
#6935=PRESENTATION_STYLE_ASSIGNMENT((#6934));
ENDSEC;
END-ISO-10303-21;
